ISO-10303-21;
HEADER;
/* Generated by software containing ST-Developer
 * from STEP Tools, Inc. (www.steptools.com) 
 */

FILE_DESCRIPTION(
/* description */ ('Ball-type isolation valve (generic)'),
/* implementation_level */ '2;1');

FILE_NAME(
/* name */ 'M5x70 body screw.step',
/* time_stamp */ '2026-10-27T10:53:05-07:00',
/* author */ (''),
/* organization */ (''),
/* preprocessor_version */ 'ST-DEVELOPER v20.2',
/* originating_system */ 'Autodesk Translation Framework v15.17.0.0',
/* authorisation */ '');

FILE_SCHEMA (('AUTOMOTIVE_DESIGN { 1 0 10303 214 3 1 1 }'));
ENDSEC;

DATA;
#10=MECHANICAL_DESIGN_GEOMETRIC_PRESENTATION_REPRESENTATION('',(#292),#7425);
#203=CONICAL_SURFACE('',#4660,0.4,0.785398163397448);
#204=CONICAL_SURFACE('',#4664,0.41,0.785398163397448);
#205=CONICAL_SURFACE('',#4668,0.26,0.463647609000806);
#218=ORIENTED_CLOSED_SHELL('',*,#4097,.F.);
#221=BREP_WITH_VOIDS('Body1',#4098,(#218));
#240=SHAPE_REPRESENTATION_RELATIONSHIP('SRR','None',#7550,#266);
#266=ADVANCED_BREP_SHAPE_REPRESENTATION('',(#221),#7413);
#292=STYLED_ITEM('',(#7751),#221);
#399=FACE_BOUND('',#1023,.T.);
#400=FACE_BOUND('',#1031,.T.);
#482=PLANE('',#4644);
#483=PLANE('',#4645);
#484=PLANE('',#4646);
#485=PLANE('',#4647);
#486=PLANE('',#4648);
#487=PLANE('',#4649);
#488=PLANE('',#4650);
#489=PLANE('',#4651);
#490=PLANE('',#4652);
#491=PLANE('',#4657);
#492=PLANE('',#4658);
#493=PLANE('',#4666);
#697=FACE_OUTER_BOUND('',#1014,.T.);
#698=FACE_OUTER_BOUND('',#1015,.T.);
#699=FACE_OUTER_BOUND('',#1016,.T.);
#700=FACE_OUTER_BOUND('',#1017,.T.);
#701=FACE_OUTER_BOUND('',#1018,.T.);
#702=FACE_OUTER_BOUND('',#1019,.T.);
#703=FACE_OUTER_BOUND('',#1020,.T.);
#704=FACE_OUTER_BOUND('',#1021,.T.);
#705=FACE_OUTER_BOUND('',#1022,.T.);
#706=FACE_OUTER_BOUND('',#1024,.T.);
#707=FACE_OUTER_BOUND('',#1025,.T.);
#708=FACE_OUTER_BOUND('',#1026,.T.);
#709=FACE_OUTER_BOUND('',#1027,.T.);
#710=FACE_OUTER_BOUND('',#1028,.T.);
#711=FACE_OUTER_BOUND('',#1029,.T.);
#712=FACE_OUTER_BOUND('',#1030,.T.);
#713=FACE_OUTER_BOUND('',#1032,.T.);
#714=FACE_OUTER_BOUND('',#1033,.T.);
#1014=EDGE_LOOP('',(#3237,#3238,#3239,#3240));
#1015=EDGE_LOOP('',(#3241,#3242,#3243,#3244));
#1016=EDGE_LOOP('',(#3245,#3246,#3247,#3248));
#1017=EDGE_LOOP('',(#3249,#3250,#3251,#3252));
#1018=EDGE_LOOP('',(#3253,#3254,#3255,#3256));
#1019=EDGE_LOOP('',(#3257,#3258,#3259,#3260));
#1020=EDGE_LOOP('',(#3261,#3262,#3263,#3264,#3265,#3266));
#1021=EDGE_LOOP('',(#3267,#3268,#3269,#3270,#3271,#3272));
#1022=EDGE_LOOP('',(#3273));
#1023=EDGE_LOOP('',(#3274));
#1024=EDGE_LOOP('',(#3275,#3276,#3277,#3278));
#1025=EDGE_LOOP('',(#3279));
#1026=EDGE_LOOP('',(#3280));
#1027=EDGE_LOOP('',(#3281,#3282,#3283,#3284));
#1028=EDGE_LOOP('',(#3285,#3286,#3287,#3288));
#1029=EDGE_LOOP('',(#3289,#3290,#3291,#3292));
#1030=EDGE_LOOP('',(#3293));
#1031=EDGE_LOOP('',(#3294));
#1032=EDGE_LOOP('',(#3295,#3296,#3297,#3298));
#1033=EDGE_LOOP('',(#3299,#3300,#3301,#3302));
#1286=LINE('',#6725,#1594);
#1287=LINE('',#6727,#1595);
#1288=LINE('',#6729,#1596);
#1289=LINE('',#6730,#1597);
#1290=LINE('',#6733,#1598);
#1291=LINE('',#6735,#1599);
#1292=LINE('',#6736,#1600);
#1293=LINE('',#6739,#1601);
#1294=LINE('',#6741,#1602);
#1295=LINE('',#6742,#1603);
#1296=LINE('',#6745,#1604);
#1297=LINE('',#6747,#1605);
#1298=LINE('',#6748,#1606);
#1299=LINE('',#6751,#1607);
#1300=LINE('',#6753,#1608);
#1301=LINE('',#6754,#1609);
#1302=LINE('',#6756,#1610);
#1303=LINE('',#6757,#1611);
#1304=LINE('',#6767,#1612);
#1305=LINE('',#6776,#1613);
#1306=LINE('',#6780,#1614);
#1307=LINE('',#6784,#1615);
#1308=LINE('',#6791,#1616);
#1309=LINE('',#6793,#1617);
#1594=VECTOR('',#5511,1.);
#1595=VECTOR('',#5512,1.);
#1596=VECTOR('',#5513,1.);
#1597=VECTOR('',#5514,1.);
#1598=VECTOR('',#5517,1.);
#1599=VECTOR('',#5518,1.);
#1600=VECTOR('',#5519,1.);
#1601=VECTOR('',#5522,1.);
#1602=VECTOR('',#5523,1.);
#1603=VECTOR('',#5524,1.);
#1604=VECTOR('',#5527,1.);
#1605=VECTOR('',#5528,1.);
#1606=VECTOR('',#5529,1.);
#1607=VECTOR('',#5532,1.);
#1608=VECTOR('',#5533,1.);
#1609=VECTOR('',#5534,1.);
#1610=VECTOR('',#5537,1.);
#1611=VECTOR('',#5538,1.);
#1612=VECTOR('',#5551,0.25);
#1613=VECTOR('',#5564,0.4);
#1614=VECTOR('',#5569,0.425);
#1615=VECTOR('',#5574,0.41);
#1616=VECTOR('',#5583,0.26);
#1617=VECTOR('',#5586,0.25);
#1891=CIRCLE('',#4653,0.25);
#1892=CIRCLE('',#4654,0.24505);
#1893=CIRCLE('',#4656,0.25);
#1894=CIRCLE('',#4659,0.375);
#1895=CIRCLE('',#4661,0.425);
#1896=CIRCLE('',#4663,0.425);
#1897=CIRCLE('',#4665,0.395);
#1898=CIRCLE('',#4667,0.27);
#1899=CIRCLE('',#4669,0.24505);
#2111=VERTEX_POINT('',#6723);
#2112=VERTEX_POINT('',#6724);
#2113=VERTEX_POINT('',#6726);
#2114=VERTEX_POINT('',#6728);
#2115=VERTEX_POINT('',#6732);
#2116=VERTEX_POINT('',#6734);
#2117=VERTEX_POINT('',#6738);
#2118=VERTEX_POINT('',#6740);
#2119=VERTEX_POINT('',#6744);
#2120=VERTEX_POINT('',#6746);
#2121=VERTEX_POINT('',#6750);
#2122=VERTEX_POINT('',#6752);
#2123=VERTEX_POINT('',#6761);
#2124=VERTEX_POINT('',#6763);
#2125=VERTEX_POINT('',#6766);
#2126=VERTEX_POINT('',#6771);
#2127=VERTEX_POINT('',#6774);
#2128=VERTEX_POINT('',#6778);
#2129=VERTEX_POINT('',#6782);
#2130=VERTEX_POINT('',#6786);
#2131=VERTEX_POINT('',#6789);
#2511=EDGE_CURVE('',#2111,#2112,#1286,.T.);
#2512=EDGE_CURVE('',#2112,#2113,#1287,.T.);
#2513=EDGE_CURVE('',#2113,#2114,#1288,.T.);
#2514=EDGE_CURVE('',#2111,#2114,#1289,.T.);
#2515=EDGE_CURVE('',#2112,#2115,#1290,.T.);
#2516=EDGE_CURVE('',#2115,#2116,#1291,.T.);
#2517=EDGE_CURVE('',#2116,#2113,#1292,.T.);
#2518=EDGE_CURVE('',#2115,#2117,#1293,.T.);
#2519=EDGE_CURVE('',#2117,#2118,#1294,.T.);
#2520=EDGE_CURVE('',#2118,#2116,#1295,.T.);
#2521=EDGE_CURVE('',#2117,#2119,#1296,.T.);
#2522=EDGE_CURVE('',#2119,#2120,#1297,.T.);
#2523=EDGE_CURVE('',#2120,#2118,#1298,.T.);
#2524=EDGE_CURVE('',#2119,#2121,#1299,.T.);
#2525=EDGE_CURVE('',#2121,#2122,#1300,.T.);
#2526=EDGE_CURVE('',#2122,#2120,#1301,.T.);
#2527=EDGE_CURVE('',#2121,#2111,#1302,.T.);
#2528=EDGE_CURVE('',#2114,#2122,#1303,.T.);
#2529=EDGE_CURVE('',#2123,#2123,#1891,.T.);
#2530=EDGE_CURVE('',#2124,#2124,#1892,.T.);
#2531=EDGE_CURVE('',#2123,#2125,#1304,.T.);
#2532=EDGE_CURVE('',#2125,#2125,#1893,.T.);
#2533=EDGE_CURVE('',#2126,#2126,#1894,.T.);
#2534=EDGE_CURVE('',#2127,#2127,#1895,.T.);
#2535=EDGE_CURVE('',#2127,#2126,#1305,.T.);
#2536=EDGE_CURVE('',#2128,#2128,#1896,.T.);
#2537=EDGE_CURVE('',#2128,#2127,#1306,.T.);
#2538=EDGE_CURVE('',#2129,#2129,#1897,.T.);
#2539=EDGE_CURVE('',#2129,#2128,#1307,.T.);
#2540=EDGE_CURVE('',#2130,#2130,#1898,.T.);
#2541=EDGE_CURVE('',#2131,#2131,#1899,.F.);
#2542=EDGE_CURVE('',#2131,#2130,#1308,.T.);
#2543=EDGE_CURVE('',#2124,#2131,#1309,.T.);
#3237=ORIENTED_EDGE('',*,*,#2511,.T.);
#3238=ORIENTED_EDGE('',*,*,#2512,.T.);
#3239=ORIENTED_EDGE('',*,*,#2513,.T.);
#3240=ORIENTED_EDGE('',*,*,#2514,.F.);
#3241=ORIENTED_EDGE('',*,*,#2515,.T.);
#3242=ORIENTED_EDGE('',*,*,#2516,.T.);
#3243=ORIENTED_EDGE('',*,*,#2517,.T.);
#3244=ORIENTED_EDGE('',*,*,#2512,.F.);
#3245=ORIENTED_EDGE('',*,*,#2518,.T.);
#3246=ORIENTED_EDGE('',*,*,#2519,.T.);
#3247=ORIENTED_EDGE('',*,*,#2520,.T.);
#3248=ORIENTED_EDGE('',*,*,#2516,.F.);
#3249=ORIENTED_EDGE('',*,*,#2521,.T.);
#3250=ORIENTED_EDGE('',*,*,#2522,.T.);
#3251=ORIENTED_EDGE('',*,*,#2523,.T.);
#3252=ORIENTED_EDGE('',*,*,#2519,.F.);
#3253=ORIENTED_EDGE('',*,*,#2524,.T.);
#3254=ORIENTED_EDGE('',*,*,#2525,.T.);
#3255=ORIENTED_EDGE('',*,*,#2526,.T.);
#3256=ORIENTED_EDGE('',*,*,#2522,.F.);
#3257=ORIENTED_EDGE('',*,*,#2527,.T.);
#3258=ORIENTED_EDGE('',*,*,#2514,.T.);
#3259=ORIENTED_EDGE('',*,*,#2528,.T.);
#3260=ORIENTED_EDGE('',*,*,#2525,.F.);
#3261=ORIENTED_EDGE('',*,*,#2527,.F.);
#3262=ORIENTED_EDGE('',*,*,#2524,.F.);
#3263=ORIENTED_EDGE('',*,*,#2521,.F.);
#3264=ORIENTED_EDGE('',*,*,#2518,.F.);
#3265=ORIENTED_EDGE('',*,*,#2515,.F.);
#3266=ORIENTED_EDGE('',*,*,#2511,.F.);
#3267=ORIENTED_EDGE('',*,*,#2528,.F.);
#3268=ORIENTED_EDGE('',*,*,#2513,.F.);
#3269=ORIENTED_EDGE('',*,*,#2517,.F.);
#3270=ORIENTED_EDGE('',*,*,#2520,.F.);
#3271=ORIENTED_EDGE('',*,*,#2523,.F.);
#3272=ORIENTED_EDGE('',*,*,#2526,.F.);
#3273=ORIENTED_EDGE('',*,*,#2529,.T.);
#3274=ORIENTED_EDGE('',*,*,#2530,.F.);
#3275=ORIENTED_EDGE('',*,*,#2529,.F.);
#3276=ORIENTED_EDGE('',*,*,#2531,.T.);
#3277=ORIENTED_EDGE('',*,*,#2532,.T.);
#3278=ORIENTED_EDGE('',*,*,#2531,.F.);
#3279=ORIENTED_EDGE('',*,*,#2532,.F.);
#3280=ORIENTED_EDGE('',*,*,#2533,.F.);
#3281=ORIENTED_EDGE('',*,*,#2534,.F.);
#3282=ORIENTED_EDGE('',*,*,#2535,.T.);
#3283=ORIENTED_EDGE('',*,*,#2533,.T.);
#3284=ORIENTED_EDGE('',*,*,#2535,.F.);
#3285=ORIENTED_EDGE('',*,*,#2536,.F.);
#3286=ORIENTED_EDGE('',*,*,#2537,.T.);
#3287=ORIENTED_EDGE('',*,*,#2534,.T.);
#3288=ORIENTED_EDGE('',*,*,#2537,.F.);
#3289=ORIENTED_EDGE('',*,*,#2538,.F.);
#3290=ORIENTED_EDGE('',*,*,#2539,.T.);
#3291=ORIENTED_EDGE('',*,*,#2536,.T.);
#3292=ORIENTED_EDGE('',*,*,#2539,.F.);
#3293=ORIENTED_EDGE('',*,*,#2538,.T.);
#3294=ORIENTED_EDGE('',*,*,#2540,.F.);
#3295=ORIENTED_EDGE('',*,*,#2541,.F.);
#3296=ORIENTED_EDGE('',*,*,#2542,.T.);
#3297=ORIENTED_EDGE('',*,*,#2540,.T.);
#3298=ORIENTED_EDGE('',*,*,#2542,.F.);
#3299=ORIENTED_EDGE('',*,*,#2530,.T.);
#3300=ORIENTED_EDGE('',*,*,#2543,.T.);
#3301=ORIENTED_EDGE('',*,*,#2541,.T.);
#3302=ORIENTED_EDGE('',*,*,#2543,.F.);
#3815=CYLINDRICAL_SURFACE('',#4655,0.25);
#3816=CYLINDRICAL_SURFACE('',#4662,0.425);
#3817=CYLINDRICAL_SURFACE('',#4670,0.24505);
#3951=ADVANCED_FACE('',(#697),#482,.F.);
#3952=ADVANCED_FACE('',(#698),#483,.F.);
#3953=ADVANCED_FACE('',(#699),#484,.F.);
#3954=ADVANCED_FACE('',(#700),#485,.F.);
#3955=ADVANCED_FACE('',(#701),#486,.F.);
#3956=ADVANCED_FACE('',(#702),#487,.F.);
#3957=ADVANCED_FACE('',(#703),#488,.F.);
#3958=ADVANCED_FACE('',(#704),#489,.F.);
#3959=ADVANCED_FACE('',(#705,#399),#490,.T.);
#3960=ADVANCED_FACE('',(#706),#3815,.T.);
#3961=ADVANCED_FACE('',(#707),#491,.F.);
#3962=ADVANCED_FACE('',(#708),#492,.T.);
#3963=ADVANCED_FACE('',(#709),#203,.T.);
#3964=ADVANCED_FACE('',(#710),#3816,.T.);
#3965=ADVANCED_FACE('',(#711),#204,.T.);
#3966=ADVANCED_FACE('',(#712,#400),#493,.T.);
#3967=ADVANCED_FACE('',(#713),#205,.T.);
#3968=ADVANCED_FACE('',(#714),#3817,.T.);
#4097=CLOSED_SHELL('',(#3951,#3952,#3953,#3954,#3955,#3956,#3957,#3958));
#4098=CLOSED_SHELL('',(#3959,#3960,#3961,#3962,#3963,#3964,#3965,#3966,
#3967,#3968));
#4643=AXIS2_PLACEMENT_3D('',#6721,#5507,#5508);
#4644=AXIS2_PLACEMENT_3D('',#6722,#5509,#5510);
#4645=AXIS2_PLACEMENT_3D('',#6731,#5515,#5516);
#4646=AXIS2_PLACEMENT_3D('',#6737,#5520,#5521);
#4647=AXIS2_PLACEMENT_3D('',#6743,#5525,#5526);
#4648=AXIS2_PLACEMENT_3D('',#6749,#5530,#5531);
#4649=AXIS2_PLACEMENT_3D('',#6755,#5535,#5536);
#4650=AXIS2_PLACEMENT_3D('',#6758,#5539,#5540);
#4651=AXIS2_PLACEMENT_3D('',#6759,#5541,#5542);
#4652=AXIS2_PLACEMENT_3D('',#6760,#5543,#5544);
#4653=AXIS2_PLACEMENT_3D('',#6762,#5545,#5546);
#4654=AXIS2_PLACEMENT_3D('',#6764,#5547,#5548);
#4655=AXIS2_PLACEMENT_3D('',#6765,#5549,#5550);
#4656=AXIS2_PLACEMENT_3D('',#6768,#5552,#5553);
#4657=AXIS2_PLACEMENT_3D('',#6769,#5554,#5555);
#4658=AXIS2_PLACEMENT_3D('',#6770,#5556,#5557);
#4659=AXIS2_PLACEMENT_3D('',#6772,#5558,#5559);
#4660=AXIS2_PLACEMENT_3D('',#6773,#5560,#5561);
#4661=AXIS2_PLACEMENT_3D('',#6775,#5562,#5563);
#4662=AXIS2_PLACEMENT_3D('',#6777,#5565,#5566);
#4663=AXIS2_PLACEMENT_3D('',#6779,#5567,#5568);
#4664=AXIS2_PLACEMENT_3D('',#6781,#5570,#5571);
#4665=AXIS2_PLACEMENT_3D('',#6783,#5572,#5573);
#4666=AXIS2_PLACEMENT_3D('',#6785,#5575,#5576);
#4667=AXIS2_PLACEMENT_3D('',#6787,#5577,#5578);
#4668=AXIS2_PLACEMENT_3D('',#6788,#5579,#5580);
#4669=AXIS2_PLACEMENT_3D('',#6790,#5581,#5582);
#4670=AXIS2_PLACEMENT_3D('',#6792,#5584,#5585);
#5507=DIRECTION('axis',(0.,0.,1.));
#5508=DIRECTION('refdir',(1.,0.,0.));
#5509=DIRECTION('center_axis',(0.866025403784439,0.,-0.5));
#5510=DIRECTION('ref_axis',(0.5,0.,0.866025403784439));
#5511=DIRECTION('',(-0.5,0.,-0.866025403784439));
#5512=DIRECTION('',(0.,-1.,0.));
#5513=DIRECTION('',(0.5,0.,0.866025403784439));
#5514=DIRECTION('',(0.,-1.,0.));
#5515=DIRECTION('center_axis',(1.20185167898973E-16,0.,-1.));
#5516=DIRECTION('ref_axis',(1.,0.,1.20185167898973E-16));
#5517=DIRECTION('',(-1.,0.,-1.20185167898973E-16));
#5518=DIRECTION('',(0.,-1.,0.));
#5519=DIRECTION('',(1.,0.,1.20185167898973E-16));
#5520=DIRECTION('center_axis',(-0.866025403784439,0.,-0.5));
#5521=DIRECTION('ref_axis',(0.5,0.,-0.866025403784439));
#5522=DIRECTION('',(-0.5,0.,0.866025403784439));
#5523=DIRECTION('',(0.,-1.,0.));
#5524=DIRECTION('',(0.5,0.,-0.866025403784439));
#5525=DIRECTION('center_axis',(-0.866025403784439,0.,0.5));
#5526=DIRECTION('ref_axis',(-0.5,0.,-0.866025403784439));
#5527=DIRECTION('',(0.5,0.,0.866025403784439));
#5528=DIRECTION('',(0.,-1.,0.));
#5529=DIRECTION('',(-0.5,0.,-0.866025403784439));
#5530=DIRECTION('center_axis',(-2.40370335797945E-16,0.,1.));
#5531=DIRECTION('ref_axis',(-1.,0.,-2.40370335797945E-16));
#5532=DIRECTION('',(1.,0.,2.40370335797945E-16));
#5533=DIRECTION('',(0.,-1.,0.));
#5534=DIRECTION('',(-1.,0.,-2.40370335797945E-16));
#5535=DIRECTION('center_axis',(0.866025403784439,0.,0.5));
#5536=DIRECTION('ref_axis',(-0.5,0.,0.866025403784439));
#5537=DIRECTION('',(0.5,0.,-0.866025403784439));
#5538=DIRECTION('',(-0.5,0.,0.866025403784439));
#5539=DIRECTION('center_axis',(0.,1.,0.));
#5540=DIRECTION('ref_axis',(1.,0.,0.));
#5541=DIRECTION('center_axis',(0.,-1.,0.));
#5542=DIRECTION('ref_axis',(0.,0.,-1.));
#5543=DIRECTION('center_axis',(0.,1.,0.));
#5544=DIRECTION('ref_axis',(1.,0.,0.));
#5545=DIRECTION('center_axis',(0.,1.,0.));
#5546=DIRECTION('ref_axis',(1.,0.,0.));
#5547=DIRECTION('center_axis',(0.,1.,0.));
#5548=DIRECTION('ref_axis',(1.,0.,0.));
#5549=DIRECTION('center_axis',(0.,1.,0.));
#5550=DIRECTION('ref_axis',(1.,0.,0.));
#5551=DIRECTION('',(0.,-1.,0.));
#5552=DIRECTION('center_axis',(0.,1.,0.));
#5553=DIRECTION('ref_axis',(1.,0.,0.));
#5554=DIRECTION('center_axis',(0.,1.,0.));
#5555=DIRECTION('ref_axis',(1.,0.,0.));
#5556=DIRECTION('center_axis',(0.,1.,0.));
#5557=DIRECTION('ref_axis',(0.,0.,1.));
#5558=DIRECTION('center_axis',(0.,-1.,0.));
#5559=DIRECTION('ref_axis',(1.,0.,0.));
#5560=DIRECTION('center_axis',(0.,-1.,0.));
#5561=DIRECTION('ref_axis',(1.,0.,0.));
#5562=DIRECTION('center_axis',(0.,-1.,0.));
#5563=DIRECTION('ref_axis',(1.,0.,0.));
#5564=DIRECTION('',(0.707106781186548,0.707106781186547,8.65956056235493E-17));
#5565=DIRECTION('center_axis',(0.,-1.,0.));
#5566=DIRECTION('ref_axis',(1.,0.,0.));
#5567=DIRECTION('center_axis',(0.,-1.,0.));
#5568=DIRECTION('ref_axis',(1.,0.,0.));
#5569=DIRECTION('',(0.,1.,0.));
#5570=DIRECTION('center_axis',(0.,1.,0.));
#5571=DIRECTION('ref_axis',(1.,0.,0.));
#5572=DIRECTION('center_axis',(0.,-1.,0.));
#5573=DIRECTION('ref_axis',(1.,0.,0.));
#5574=DIRECTION('',(-0.707106781186547,0.707106781186548,-8.65956056235493E-17));
#5575=DIRECTION('center_axis',(0.,-1.,0.));
#5576=DIRECTION('ref_axis',(0.,0.,-1.));
#5577=DIRECTION('center_axis',(0.,-1.,0.));
#5578=DIRECTION('ref_axis',(1.,0.,0.));
#5579=DIRECTION('center_axis',(0.,1.,0.));
#5580=DIRECTION('ref_axis',(1.,0.,0.));
#5581=DIRECTION('center_axis',(0.,1.,0.));
#5582=DIRECTION('ref_axis',(1.,0.,0.));
#5583=DIRECTION('',(-0.447213595499958,0.894427190999916,-5.47678698264203E-17));
#5584=DIRECTION('center_axis',(0.,-1.,0.));
#5585=DIRECTION('ref_axis',(1.,0.,0.));
#5586=DIRECTION('',(0.,1.,0.));
#6721=CARTESIAN_POINT('',(0.,0.,0.));
#6722=CARTESIAN_POINT('Origin',(0.115470053837925,-0.5,-0.2));
#6723=CARTESIAN_POINT('',(0.23094010767585,-0.5,0.));
#6724=CARTESIAN_POINT('',(0.115470053837925,-0.5,-0.2));
#6725=CARTESIAN_POINT('',(0.23094010767585,-0.5,0.));
#6726=CARTESIAN_POINT('',(0.115470053837925,-0.8,-0.2));
#6727=CARTESIAN_POINT('',(0.115470053837925,-0.5,-0.2));
#6728=CARTESIAN_POINT('',(0.23094010767585,-0.8,0.));
#6729=CARTESIAN_POINT('',(0.23094010767585,-0.8,0.));
#6730=CARTESIAN_POINT('',(0.23094010767585,-0.5,0.));
#6731=CARTESIAN_POINT('Origin',(-0.115470053837925,-0.5,-0.2));
#6732=CARTESIAN_POINT('',(-0.115470053837925,-0.5,-0.2));
#6733=CARTESIAN_POINT('',(0.115470053837925,-0.5,-0.2));
#6734=CARTESIAN_POINT('',(-0.115470053837925,-0.8,-0.2));
#6735=CARTESIAN_POINT('',(-0.115470053837925,-0.5,-0.2));
#6736=CARTESIAN_POINT('',(0.115470053837925,-0.8,-0.2));
#6737=CARTESIAN_POINT('Origin',(-0.23094010767585,-0.5,-2.77555756156289E-17));
#6738=CARTESIAN_POINT('',(-0.23094010767585,-0.5,-2.82820063659975E-17));
#6739=CARTESIAN_POINT('',(-0.115470053837925,-0.5,-0.2));
#6740=CARTESIAN_POINT('',(-0.23094010767585,-0.8,-2.77555756156289E-17));
#6741=CARTESIAN_POINT('',(-0.23094010767585,-0.5,-2.82820063659975E-17));
#6742=CARTESIAN_POINT('',(-0.115470053837925,-0.8,-0.2));
#6743=CARTESIAN_POINT('Origin',(-0.115470053837925,-0.5,0.2));
#6744=CARTESIAN_POINT('',(-0.115470053837925,-0.5,0.2));
#6745=CARTESIAN_POINT('',(-0.23094010767585,-0.5,-2.82820063659975E-17));
#6746=CARTESIAN_POINT('',(-0.115470053837925,-0.8,0.2));
#6747=CARTESIAN_POINT('',(-0.115470053837925,-0.5,0.2));
#6748=CARTESIAN_POINT('',(-0.23094010767585,-0.8,-2.82820063659975E-17));
#6749=CARTESIAN_POINT('Origin',(0.115470053837925,-0.5,0.2));
#6750=CARTESIAN_POINT('',(0.115470053837925,-0.5,0.2));
#6751=CARTESIAN_POINT('',(-0.115470053837925,-0.5,0.2));
#6752=CARTESIAN_POINT('',(0.115470053837925,-0.8,0.2));
#6753=CARTESIAN_POINT('',(0.115470053837925,-0.5,0.2));
#6754=CARTESIAN_POINT('',(-0.115470053837925,-0.8,0.2));
#6755=CARTESIAN_POINT('Origin',(0.23094010767585,-0.5,0.));
#6756=CARTESIAN_POINT('',(0.115470053837925,-0.5,0.2));
#6757=CARTESIAN_POINT('',(0.115470053837925,-0.8,0.2));
#6758=CARTESIAN_POINT('Origin',(0.,-0.5,0.));
#6759=CARTESIAN_POINT('Origin',(0.,-0.8,0.));
#6760=CARTESIAN_POINT('Origin',(0.,-1.9,0.));
#6761=CARTESIAN_POINT('',(-0.25,-1.9,3.06161699786838E-17));
#6762=CARTESIAN_POINT('Origin',(0.,-1.9,0.));
#6763=CARTESIAN_POINT('',(-0.24505,-1.9,3.00099698131059E-17));
#6764=CARTESIAN_POINT('Origin',(0.,-1.9,0.));
#6765=CARTESIAN_POINT('Origin',(0.,-7.,0.));
#6766=CARTESIAN_POINT('',(-0.25,-7.,3.06161699786838E-17));
#6767=CARTESIAN_POINT('',(-0.25,-7.,3.06161699786838E-17));
#6768=CARTESIAN_POINT('Origin',(0.,-7.,0.));
#6769=CARTESIAN_POINT('Origin',(0.,-7.,0.));
#6770=CARTESIAN_POINT('Origin',(0.375,0.5,0.));
#6771=CARTESIAN_POINT('',(-0.375,0.5,-4.59242549680257E-17));
#6772=CARTESIAN_POINT('Origin',(0.,0.5,0.));
#6773=CARTESIAN_POINT('Origin',(0.,0.475,0.));
#6774=CARTESIAN_POINT('',(-0.425,0.45,-5.20474889637625E-17));
#6775=CARTESIAN_POINT('Origin',(0.,0.45,0.));
#6776=CARTESIAN_POINT('',(-0.4,0.475,-4.89858719658941E-17));
#6777=CARTESIAN_POINT('Origin',(0.,0.24,0.));
#6778=CARTESIAN_POINT('',(-0.425,0.0299999999999998,-5.20474889637625E-17));
#6779=CARTESIAN_POINT('Origin',(0.,0.0299999999999998,0.));
#6780=CARTESIAN_POINT('',(-0.425,0.24,-5.20474889637625E-17));
#6781=CARTESIAN_POINT('Origin',(0.,0.0150000000000001,0.));
#6782=CARTESIAN_POINT('',(-0.395,4.85722573273506E-17,-4.83735485663204E-17));
#6783=CARTESIAN_POINT('Origin',(0.,0.,0.));
#6784=CARTESIAN_POINT('',(-0.41,0.0150000000000001,-5.02105187650415E-17));
#6785=CARTESIAN_POINT('Origin',(0.27,0.,0.));
#6786=CARTESIAN_POINT('',(-0.27,0.,-3.30654635769785E-17));
#6787=CARTESIAN_POINT('Origin',(0.,0.,0.));
#6788=CARTESIAN_POINT('Origin',(0.,-0.02,0.));
#6789=CARTESIAN_POINT('',(-0.24505,-0.0498999999999999,3.00099698131059E-17));
#6790=CARTESIAN_POINT('Origin',(0.,-0.0498999999999999,0.));
#6791=CARTESIAN_POINT('',(-0.26,-0.02,-3.18408167778312E-17));
#6792=CARTESIAN_POINT('Origin',(0.,-0.995,0.));
#6793=CARTESIAN_POINT('',(-0.24505,-0.995,-3.00099698131059E-17));
#7383=UNCERTAINTY_MEASURE_WITH_UNIT(LENGTH_MEASURE(0.001),#7426,
'DISTANCE_ACCURACY_VALUE',
'Maximum model space distance between geometric entities at asserted c
onnectivities');
#7395=UNCERTAINTY_MEASURE_WITH_UNIT(LENGTH_MEASURE(0.001),#7426,
'DISTANCE_ACCURACY_VALUE',
'Maximum model space distance between geometric entities at asserted c
onnectivities');
#7413=(
GEOMETRIC_REPRESENTATION_CONTEXT(3)
GLOBAL_UNCERTAINTY_ASSIGNED_CONTEXT((#7383))
GLOBAL_UNIT_ASSIGNED_CONTEXT((#7426,#7428,#7429))
REPRESENTATION_CONTEXT('','3D')
);
#7425=(
GEOMETRIC_REPRESENTATION_CONTEXT(3)
GLOBAL_UNCERTAINTY_ASSIGNED_CONTEXT((#7395))
GLOBAL_UNIT_ASSIGNED_CONTEXT((#7426,#7428,#7429))
REPRESENTATION_CONTEXT('','3D')
);
#7426=(
LENGTH_UNIT()
NAMED_UNIT(*)
SI_UNIT(.CENTI.,.METRE.)
);
#7428=(
NAMED_UNIT(*)
PLANE_ANGLE_UNIT()
SI_UNIT($,.RADIAN.)
);
#7429=(
NAMED_UNIT(*)
SI_UNIT($,.STERADIAN.)
SOLID_ANGLE_UNIT()
);
#7447=SHAPE_DEFINITION_REPRESENTATION(#7476,#7550);
#7476=PRODUCT_DEFINITION_SHAPE('',$,#7580);
#7550=SHAPE_REPRESENTATION('',(#4643),#7413);
#7562=PRODUCT_DEFINITION_CONTEXT('part definition',#7651,'design');
#7580=PRODUCT_DEFINITION('M5x70 body screw','M5x70 body screw',#7609,#7562);
#7609=PRODUCT_DEFINITION_FORMATION('',$,#7670);
#7651=APPLICATION_CONTEXT(
'Core Data for Automotive Mechanical Design Process');
#7652=PRODUCT_CONTEXT('part definition',#7651,'mechanical');
#7670=PRODUCT('M5x70 body screw','M5x70 body screw','M5x70 body screw',
(#7652));
#7745=COLOUR_RGB('Black',0.12,0.14,0.17);
#7746=FILL_AREA_STYLE_COLOUR('',#7745);
#7747=FILL_AREA_STYLE('',(#7746));
#7748=SURFACE_STYLE_FILL_AREA(#7747);
#7749=SURFACE_SIDE_STYLE('',(#7748));
#7750=SURFACE_STYLE_USAGE(.BOTH.,#7749);
#7751=PRESENTATION_STYLE_ASSIGNMENT((#7750));
ENDSEC;
END-ISO-10303-21;
